ISO-10303-21;
HEADER;
/* Generated by software containing ST-Developer
 * from STEP Tools, Inc. (www.steptools.com) 
 */

FILE_DESCRIPTION(
/* description */ ('STEP AP203'),
/* implementation_level */ '2;1');

FILE_NAME(
/* name */ 'P11_Upper_Feed_Screw.step',
/* time_stamp */ '2026-11-15T15:04:01-08:00',
/* author */ (''),
/* organization */ (''),
/* preprocessor_version */ 'ST-DEVELOPER v20.2',
/* originating_system */ 'Autodesk Translation Framework v15.17.0.0',
/* authorisation */ '');

FILE_SCHEMA (('AUTOMOTIVE_DESIGN { 1 0 10303 214 3 1 1 }'));
ENDSEC;

DATA;
#10=MECHANICAL_DESIGN_GEOMETRIC_PRESENTATION_REPRESENTATION('',(#290),#16598);
#212=SHAPE_REPRESENTATION_RELATIONSHIP('SRR','None',#16706,#236);
#236=ADVANCED_BREP_SHAPE_REPRESENTATION('',(#260),#16582);
#260=MANIFOLD_SOLID_BREP('Body1',#9795);
#290=STYLED_ITEM('',(#16832),#260);
#346=FACE_BOUND('',#1710,.T.);
#347=FACE_BOUND('',#1712,.T.);
#348=FACE_BOUND('',#1714,.T.);
#349=FACE_BOUND('',#1716,.T.);
#601=PLANE('',#10372);
#602=PLANE('',#10373);
#603=PLANE('',#10374);
#604=PLANE('',#10375);
#605=PLANE('',#10376);
#606=PLANE('',#10377);
#1112=FACE_OUTER_BOUND('',#1703,.T.);
#1113=FACE_OUTER_BOUND('',#1704,.T.);
#1114=FACE_OUTER_BOUND('',#1705,.T.);
#1115=FACE_OUTER_BOUND('',#1706,.T.);
#1116=FACE_OUTER_BOUND('',#1707,.T.);
#1117=FACE_OUTER_BOUND('',#1708,.T.);
#1118=FACE_OUTER_BOUND('',#1709,.T.);
#1119=FACE_OUTER_BOUND('',#1711,.T.);
#1120=FACE_OUTER_BOUND('',#1713,.T.);
#1121=FACE_OUTER_BOUND('',#1715,.T.);
#1122=FACE_OUTER_BOUND('',#1717,.T.);
#1703=EDGE_LOOP('',(#7587,#7588,#7589,#7590));
#1704=EDGE_LOOP('',(#7591,#7592,#7593,#7594));
#1705=EDGE_LOOP('',(#7595,#7596,#7597,#7598));
#1706=EDGE_LOOP('',(#7599,#7600,#7601,#7602));
#1707=EDGE_LOOP('',(#7603,#7604,#7605,#7606));
#1708=EDGE_LOOP('',(#7607));
#1709=EDGE_LOOP('',(#7608));
#1710=EDGE_LOOP('',(#7609));
#1711=EDGE_LOOP('',(#7610));
#1712=EDGE_LOOP('',(#7611));
#1713=EDGE_LOOP('',(#7612));
#1714=EDGE_LOOP('',(#7613));
#1715=EDGE_LOOP('',(#7614));
#1716=EDGE_LOOP('',(#7615));
#1717=EDGE_LOOP('',(#7616));
#2561=LINE('',#14720,#3609);
#2562=LINE('',#14726,#3610);
#2563=LINE('',#14732,#3611);
#2564=LINE('',#14738,#3612);
#2565=LINE('',#14744,#3613);
#3609=VECTOR('',#11919,7.15);
#3610=VECTOR('',#11926,6.);
#3611=VECTOR('',#11933,9.);
#3612=VECTOR('',#11940,6.);
#3613=VECTOR('',#11947,4.);
#4293=CIRCLE('',#10358,7.15);
#4294=CIRCLE('',#10359,7.15);
#4295=CIRCLE('',#10361,6.);
#4296=CIRCLE('',#10362,6.);
#4297=CIRCLE('',#10364,9.);
#4298=CIRCLE('',#10365,9.);
#4299=CIRCLE('',#10367,6.);
#4300=CIRCLE('',#10368,6.);
#4301=CIRCLE('',#10370,4.);
#4302=CIRCLE('',#10371,4.);
#4785=VERTEX_POINT('',#14717);
#4786=VERTEX_POINT('',#14719);
#4787=VERTEX_POINT('',#14723);
#4788=VERTEX_POINT('',#14725);
#4789=VERTEX_POINT('',#14729);
#4790=VERTEX_POINT('',#14731);
#4791=VERTEX_POINT('',#14735);
#4792=VERTEX_POINT('',#14737);
#4793=VERTEX_POINT('',#14741);
#4794=VERTEX_POINT('',#14743);
#5806=EDGE_CURVE('',#4785,#4785,#4293,.T.);
#5807=EDGE_CURVE('',#4785,#4786,#2561,.T.);
#5808=EDGE_CURVE('',#4786,#4786,#4294,.T.);
#5809=EDGE_CURVE('',#4787,#4787,#4295,.T.);
#5810=EDGE_CURVE('',#4787,#4788,#2562,.T.);
#5811=EDGE_CURVE('',#4788,#4788,#4296,.T.);
#5812=EDGE_CURVE('',#4789,#4789,#4297,.T.);
#5813=EDGE_CURVE('',#4789,#4790,#2563,.T.);
#5814=EDGE_CURVE('',#4790,#4790,#4298,.T.);
#5815=EDGE_CURVE('',#4791,#4791,#4299,.T.);
#5816=EDGE_CURVE('',#4791,#4792,#2564,.T.);
#5817=EDGE_CURVE('',#4792,#4792,#4300,.T.);
#5818=EDGE_CURVE('',#4793,#4793,#4301,.T.);
#5819=EDGE_CURVE('',#4793,#4794,#2565,.T.);
#5820=EDGE_CURVE('',#4794,#4794,#4302,.T.);
#7587=ORIENTED_EDGE('',*,*,#5806,.F.);
#7588=ORIENTED_EDGE('',*,*,#5807,.T.);
#7589=ORIENTED_EDGE('',*,*,#5808,.T.);
#7590=ORIENTED_EDGE('',*,*,#5807,.F.);
#7591=ORIENTED_EDGE('',*,*,#5809,.F.);
#7592=ORIENTED_EDGE('',*,*,#5810,.T.);
#7593=ORIENTED_EDGE('',*,*,#5811,.T.);
#7594=ORIENTED_EDGE('',*,*,#5810,.F.);
#7595=ORIENTED_EDGE('',*,*,#5812,.F.);
#7596=ORIENTED_EDGE('',*,*,#5813,.T.);
#7597=ORIENTED_EDGE('',*,*,#5814,.T.);
#7598=ORIENTED_EDGE('',*,*,#5813,.F.);
#7599=ORIENTED_EDGE('',*,*,#5815,.F.);
#7600=ORIENTED_EDGE('',*,*,#5816,.T.);
#7601=ORIENTED_EDGE('',*,*,#5817,.T.);
#7602=ORIENTED_EDGE('',*,*,#5816,.F.);
#7603=ORIENTED_EDGE('',*,*,#5818,.F.);
#7604=ORIENTED_EDGE('',*,*,#5819,.T.);
#7605=ORIENTED_EDGE('',*,*,#5820,.T.);
#7606=ORIENTED_EDGE('',*,*,#5819,.F.);
#7607=ORIENTED_EDGE('',*,*,#5818,.T.);
#7608=ORIENTED_EDGE('',*,*,#5815,.T.);
#7609=ORIENTED_EDGE('',*,*,#5820,.F.);
#7610=ORIENTED_EDGE('',*,*,#5812,.T.);
#7611=ORIENTED_EDGE('',*,*,#5817,.F.);
#7612=ORIENTED_EDGE('',*,*,#5814,.F.);
#7613=ORIENTED_EDGE('',*,*,#5809,.T.);
#7614=ORIENTED_EDGE('',*,*,#5806,.T.);
#7615=ORIENTED_EDGE('',*,*,#5811,.F.);
#7616=ORIENTED_EDGE('',*,*,#5808,.F.);
#9198=CYLINDRICAL_SURFACE('',#10357,7.15);
#9199=CYLINDRICAL_SURFACE('',#10360,6.);
#9200=CYLINDRICAL_SURFACE('',#10363,9.);
#9201=CYLINDRICAL_SURFACE('',#10366,6.);
#9202=CYLINDRICAL_SURFACE('',#10369,4.);
#9437=ADVANCED_FACE('',(#1112),#9198,.T.);
#9438=ADVANCED_FACE('',(#1113),#9199,.T.);
#9439=ADVANCED_FACE('',(#1114),#9200,.T.);
#9440=ADVANCED_FACE('',(#1115),#9201,.T.);
#9441=ADVANCED_FACE('',(#1116),#9202,.T.);
#9442=ADVANCED_FACE('',(#1117),#601,.F.);
#9443=ADVANCED_FACE('',(#1118,#346),#602,.F.);
#9444=ADVANCED_FACE('',(#1119,#347),#603,.F.);
#9445=ADVANCED_FACE('',(#1120,#348),#604,.F.);
#9446=ADVANCED_FACE('',(#1121,#349),#605,.F.);
#9447=ADVANCED_FACE('',(#1122),#606,.F.);
#9795=CLOSED_SHELL('',(#9437,#9438,#9439,#9440,#9441,#9442,#9443,#9444,
#9445,#9446,#9447));
#10356=AXIS2_PLACEMENT_3D('',#14715,#11913,#11914);
#10357=AXIS2_PLACEMENT_3D('',#14716,#11915,#11916);
#10358=AXIS2_PLACEMENT_3D('',#14718,#11917,#11918);
#10359=AXIS2_PLACEMENT_3D('',#14721,#11920,#11921);
#10360=AXIS2_PLACEMENT_3D('',#14722,#11922,#11923);
#10361=AXIS2_PLACEMENT_3D('',#14724,#11924,#11925);
#10362=AXIS2_PLACEMENT_3D('',#14727,#11927,#11928);
#10363=AXIS2_PLACEMENT_3D('',#14728,#11929,#11930);
#10364=AXIS2_PLACEMENT_3D('',#14730,#11931,#11932);
#10365=AXIS2_PLACEMENT_3D('',#14733,#11934,#11935);
#10366=AXIS2_PLACEMENT_3D('',#14734,#11936,#11937);
#10367=AXIS2_PLACEMENT_3D('',#14736,#11938,#11939);
#10368=AXIS2_PLACEMENT_3D('',#14739,#11941,#11942);
#10369=AXIS2_PLACEMENT_3D('',#14740,#11943,#11944);
#10370=AXIS2_PLACEMENT_3D('',#14742,#11945,#11946);
#10371=AXIS2_PLACEMENT_3D('',#14745,#11948,#11949);
#10372=AXIS2_PLACEMENT_3D('',#14746,#11950,#11951);
#10373=AXIS2_PLACEMENT_3D('',#14747,#11952,#11953);
#10374=AXIS2_PLACEMENT_3D('',#14748,#11954,#11955);
#10375=AXIS2_PLACEMENT_3D('',#14749,#11956,#11957);
#10376=AXIS2_PLACEMENT_3D('',#14750,#11958,#11959);
#10377=AXIS2_PLACEMENT_3D('',#14751,#11960,#11961);
#11913=DIRECTION('axis',(0.,0.,1.));
#11914=DIRECTION('refdir',(1.,0.,0.));
#11915=DIRECTION('center_axis',(0.,0.,-1.));
#11916=DIRECTION('ref_axis',(-1.,0.,0.));
#11917=DIRECTION('center_axis',(0.,0.,-1.));
#11918=DIRECTION('ref_axis',(-1.,0.,0.));
#11919=DIRECTION('',(0.,0.,1.));
#11920=DIRECTION('center_axis',(0.,0.,-1.));
#11921=DIRECTION('ref_axis',(-1.,0.,0.));
#11922=DIRECTION('center_axis',(0.,0.,-1.));
#11923=DIRECTION('ref_axis',(-1.,0.,0.));
#11924=DIRECTION('center_axis',(0.,0.,-1.));
#11925=DIRECTION('ref_axis',(-1.,0.,0.));
#11926=DIRECTION('',(0.,0.,1.));
#11927=DIRECTION('center_axis',(0.,0.,-1.));
#11928=DIRECTION('ref_axis',(-1.,0.,0.));
#11929=DIRECTION('center_axis',(0.,0.,-1.));
#11930=DIRECTION('ref_axis',(-1.,0.,0.));
#11931=DIRECTION('center_axis',(0.,0.,-1.));
#11932=DIRECTION('ref_axis',(-1.,0.,0.));
#11933=DIRECTION('',(0.,0.,1.));
#11934=DIRECTION('center_axis',(0.,0.,-1.));
#11935=DIRECTION('ref_axis',(-1.,0.,0.));
#11936=DIRECTION('center_axis',(0.,0.,-1.));
#11937=DIRECTION('ref_axis',(-1.,0.,0.));
#11938=DIRECTION('center_axis',(0.,0.,-1.));
#11939=DIRECTION('ref_axis',(-1.,0.,0.));
#11940=DIRECTION('',(0.,0.,1.));
#11941=DIRECTION('center_axis',(0.,0.,-1.));
#11942=DIRECTION('ref_axis',(-1.,0.,0.));
#11943=DIRECTION('center_axis',(0.,0.,-1.));
#11944=DIRECTION('ref_axis',(-1.,0.,0.));
#11945=DIRECTION('center_axis',(0.,0.,-1.));
#11946=DIRECTION('ref_axis',(-1.,0.,0.));
#11947=DIRECTION('',(0.,0.,1.));
#11948=DIRECTION('center_axis',(0.,0.,-1.));
#11949=DIRECTION('ref_axis',(-1.,0.,0.));
#11950=DIRECTION('center_axis',(0.,0.,1.));
#11951=DIRECTION('ref_axis',(1.,0.,0.));
#11952=DIRECTION('center_axis',(0.,0.,1.));
#11953=DIRECTION('ref_axis',(1.,0.,0.));
#11954=DIRECTION('center_axis',(0.,0.,1.));
#11955=DIRECTION('ref_axis',(1.,0.,0.));
#11956=DIRECTION('center_axis',(0.,0.,-1.));
#11957=DIRECTION('ref_axis',(-1.,0.,0.));
#11958=DIRECTION('center_axis',(0.,0.,1.));
#11959=DIRECTION('ref_axis',(1.,0.,0.));
#11960=DIRECTION('center_axis',(0.,0.,-1.));
#11961=DIRECTION('ref_axis',(-1.,0.,0.));
#14715=CARTESIAN_POINT('',(0.,0.,0.));
#14716=CARTESIAN_POINT('Origin',(0.,0.,-5.));
#14717=CARTESIAN_POINT('',(7.15,-8.75622461390358E-16,46.));
#14718=CARTESIAN_POINT('Origin',(0.,0.,46.));
#14719=CARTESIAN_POINT('',(7.15,-8.75622461390358E-16,230.));
#14720=CARTESIAN_POINT('',(7.15,-8.75622461390358E-16,-5.));
#14721=CARTESIAN_POINT('Origin',(0.,0.,230.));
#14722=CARTESIAN_POINT('Origin',(0.,0.,-5.));
#14723=CARTESIAN_POINT('',(6.,-7.34788079488412E-16,40.));
#14724=CARTESIAN_POINT('Origin',(0.,0.,40.));
#14725=CARTESIAN_POINT('',(6.,-7.34788079488412E-16,46.));
#14726=CARTESIAN_POINT('',(6.,-7.34788079488412E-16,-5.));
#14727=CARTESIAN_POINT('Origin',(0.,0.,46.));
#14728=CARTESIAN_POINT('Origin',(0.,0.,-5.));
#14729=CARTESIAN_POINT('',(9.,-1.10218211923262E-15,36.));
#14730=CARTESIAN_POINT('Origin',(0.,0.,36.));
#14731=CARTESIAN_POINT('',(9.,-1.10218211923262E-15,40.));
#14732=CARTESIAN_POINT('',(9.,-1.10218211923262E-15,-5.));
#14733=CARTESIAN_POINT('Origin',(0.,0.,40.));
#14734=CARTESIAN_POINT('Origin',(0.,0.,-5.));
#14735=CARTESIAN_POINT('',(6.,-7.34788079488412E-16,14.));
#14736=CARTESIAN_POINT('Origin',(0.,0.,14.));
#14737=CARTESIAN_POINT('',(6.,-7.34788079488412E-16,36.));
#14738=CARTESIAN_POINT('',(6.,-7.34788079488412E-16,-5.));
#14739=CARTESIAN_POINT('Origin',(0.,0.,36.));
#14740=CARTESIAN_POINT('Origin',(0.,0.,-5.));
#14741=CARTESIAN_POINT('',(4.,-4.89858719658941E-16,0.));
#14742=CARTESIAN_POINT('Origin',(0.,0.,0.));
#14743=CARTESIAN_POINT('',(4.,-4.89858719658941E-16,14.));
#14744=CARTESIAN_POINT('',(4.,-4.89858719658941E-16,-5.));
#14745=CARTESIAN_POINT('Origin',(0.,0.,14.));
#14746=CARTESIAN_POINT('Origin',(0.,0.,0.));
#14747=CARTESIAN_POINT('Origin',(4.,0.,14.));
#14748=CARTESIAN_POINT('Origin',(6.,0.,36.));
#14749=CARTESIAN_POINT('Origin',(9.,0.,40.));
#14750=CARTESIAN_POINT('Origin',(6.,0.,46.));
#14751=CARTESIAN_POINT('Origin',(7.15,0.,230.));
#16556=UNCERTAINTY_MEASURE_WITH_UNIT(LENGTH_MEASURE(0.01),#16599,
'DISTANCE_ACCURACY_VALUE',
'Maximum model space distance between geometric entities at asserted c
onnectivities');
#16572=UNCERTAINTY_MEASURE_WITH_UNIT(LENGTH_MEASURE(0.01),#16599,
'DISTANCE_ACCURACY_VALUE',
'Maximum model space distance between geometric entities at asserted c
onnectivities');
#16582=(
GEOMETRIC_REPRESENTATION_CONTEXT(3)
GLOBAL_UNCERTAINTY_ASSIGNED_CONTEXT((#16556))
GLOBAL_UNIT_ASSIGNED_CONTEXT((#16599,#16601,#16602))
REPRESENTATION_CONTEXT('','3D')
);
#16598=(
GEOMETRIC_REPRESENTATION_CONTEXT(3)
GLOBAL_UNCERTAINTY_ASSIGNED_CONTEXT((#16572))
GLOBAL_UNIT_ASSIGNED_CONTEXT((#16599,#16601,#16602))
REPRESENTATION_CONTEXT('','3D')
);
#16599=(
LENGTH_UNIT()
NAMED_UNIT(*)
SI_UNIT(.MILLI.,.METRE.)
);
#16601=(
NAMED_UNIT(*)
PLANE_ANGLE_UNIT()
SI_UNIT($,.RADIAN.)
);
#16602=(
NAMED_UNIT(*)
SI_UNIT($,.STERADIAN.)
SOLID_ANGLE_UNIT()
);
#16612=SHAPE_DEFINITION_REPRESENTATION(#16637,#16706);
#16637=PRODUCT_DEFINITION_SHAPE('',$,#16732);
#16706=SHAPE_REPRESENTATION('',(#10356),#16582);
#16722=PRODUCT_DEFINITION_CONTEXT('part definition',#16799,'design');
#16732=PRODUCT_DEFINITION('P11_Upper_Feed_Screw','P11_Upper_Feed_Screw',
#16757,#16722);
#16757=PRODUCT_DEFINITION_FORMATION('',$,#16810);
#16799=APPLICATION_CONTEXT(
'Core Data for Automotive Mechanical Design Process');
#16800=PRODUCT_CONTEXT('part definition',#16799,'mechanical');
#16810=PRODUCT('P11_Upper_Feed_Screw','P11_Upper_Feed_Screw',$,(#16800));
#16832=PRESENTATION_STYLE_ASSIGNMENT((#16841));
#16841=SURFACE_STYLE_USAGE(.BOTH.,#16850);
#16850=SURFACE_SIDE_STYLE('',(#16859));
#16859=SURFACE_STYLE_FILL_AREA(#16868);
#16868=FILL_AREA_STYLE('Sky Blue',(#16877));
#16877=FILL_AREA_STYLE_COLOUR('Sky Blue',#16886);
#16886=COLOUR_RGB('Sky Blue',0.529411764705882,0.807843137254902,0.92156862745098);
ENDSEC;
END-ISO-10303-21;
